ISO-10303-21;
HEADER;
/* Generated by software containing ST-Developer
 * from STEP Tools, Inc. (www.steptools.com) 
 */

FILE_DESCRIPTION(
/* description */ ('Fatigue rig crank-slider'),
/* implementation_level */ '2;1');

FILE_NAME(
/* name */ 'Cap Screw - M5x20.step',
/* time_stamp */ '2026-10-28T03:24:50-07:00',
/* author */ (''),
/* organization */ (''),
/* preprocessor_version */ 'ST-DEVELOPER v20.2',
/* originating_system */ 'Autodesk Translation Framework v15.17.0.0',
/* authorisation */ '');

FILE_SCHEMA (('AUTOMOTIVE_DESIGN { 1 0 10303 214 3 1 1 }'));
ENDSEC;

DATA;
#10=MECHANICAL_DESIGN_GEOMETRIC_PRESENTATION_REPRESENTATION('',(#644),#16911);
#30=CONICAL_SURFACE('',#10444,0.4,0.785398163397448);
#31=CONICAL_SURFACE('',#10448,0.41,0.785398163397448);
#32=CONICAL_SURFACE('',#10452,0.26,0.463647609000806);
#33=CONICAL_SURFACE('',#10456,0.225,0.785398163397448);
#40=ORIENTED_CLOSED_SHELL('',*,#8939,.F.);
#45=BREP_WITH_VOIDS('Body1',#8938,(#40));
#535=SHAPE_REPRESENTATION_RELATIONSHIP('SRR','None',#17180,#585);
#585=ADVANCED_BREP_SHAPE_REPRESENTATION('',(#45),#16909);
#644=STYLED_ITEM('',(#17494),#45);
#895=FACE_BOUND('',#2430,.T.);
#1195=PLANE('',#10442);
#1196=PLANE('',#10450);
#1197=PLANE('',#10458);
#1198=PLANE('',#10459);
#1199=PLANE('',#10460);
#1200=PLANE('',#10461);
#1201=PLANE('',#10462);
#1202=PLANE('',#10463);
#1203=PLANE('',#10464);
#1204=PLANE('',#10465);
#1205=PLANE('',#10466);
#1707=FACE_OUTER_BOUND('',#2425,.T.);
#1708=FACE_OUTER_BOUND('',#2426,.T.);
#1709=FACE_OUTER_BOUND('',#2427,.T.);
#1710=FACE_OUTER_BOUND('',#2428,.T.);
#1711=FACE_OUTER_BOUND('',#2429,.T.);
#1712=FACE_OUTER_BOUND('',#2431,.T.);
#1713=FACE_OUTER_BOUND('',#2432,.T.);
#1714=FACE_OUTER_BOUND('',#2433,.T.);
#1715=FACE_OUTER_BOUND('',#2434,.T.);
#1716=FACE_OUTER_BOUND('',#2435,.T.);
#1717=FACE_OUTER_BOUND('',#2436,.T.);
#1718=FACE_OUTER_BOUND('',#2437,.T.);
#1719=FACE_OUTER_BOUND('',#2438,.T.);
#1720=FACE_OUTER_BOUND('',#2439,.T.);
#1721=FACE_OUTER_BOUND('',#2440,.T.);
#1722=FACE_OUTER_BOUND('',#2441,.T.);
#1723=FACE_OUTER_BOUND('',#2442,.T.);
#2425=EDGE_LOOP('',(#8072));
#2426=EDGE_LOOP('',(#8073,#8074,#8075,#8076));
#2427=EDGE_LOOP('',(#8077,#8078,#8079,#8080));
#2428=EDGE_LOOP('',(#8081,#8082,#8083,#8084));
#2429=EDGE_LOOP('',(#8085));
#2430=EDGE_LOOP('',(#8086));
#2431=EDGE_LOOP('',(#8087,#8088,#8089,#8090));
#2432=EDGE_LOOP('',(#8091,#8092,#8093,#8094));
#2433=EDGE_LOOP('',(#8095,#8096,#8097,#8098));
#2434=EDGE_LOOP('',(#8099));
#2435=EDGE_LOOP('',(#8100,#8101,#8102,#8103));
#2436=EDGE_LOOP('',(#8104,#8105,#8106,#8107));
#2437=EDGE_LOOP('',(#8108,#8109,#8110,#8111));
#2438=EDGE_LOOP('',(#8112,#8113,#8114,#8115));
#2439=EDGE_LOOP('',(#8116,#8117,#8118,#8119));
#2440=EDGE_LOOP('',(#8120,#8121,#8122,#8123));
#2441=EDGE_LOOP('',(#8124,#8125,#8126,#8127,#8128,#8129));
#2442=EDGE_LOOP('',(#8130,#8131,#8132,#8133,#8134,#8135));
#3059=LINE('',#16590,#3705);
#3060=LINE('',#16594,#3706);
#3061=LINE('',#16598,#3707);
#3062=LINE('',#16605,#3708);
#3063=LINE('',#16609,#3709);
#3064=LINE('',#16613,#3710);
#3065=LINE('',#16618,#3711);
#3066=LINE('',#16620,#3712);
#3067=LINE('',#16622,#3713);
#3068=LINE('',#16623,#3714);
#3069=LINE('',#16626,#3715);
#3070=LINE('',#16628,#3716);
#3071=LINE('',#16629,#3717);
#3072=LINE('',#16632,#3718);
#3073=LINE('',#16634,#3719);
#3074=LINE('',#16635,#3720);
#3075=LINE('',#16638,#3721);
#3076=LINE('',#16640,#3722);
#3077=LINE('',#16641,#3723);
#3078=LINE('',#16644,#3724);
#3079=LINE('',#16646,#3725);
#3080=LINE('',#16647,#3726);
#3081=LINE('',#16649,#3727);
#3082=LINE('',#16650,#3728);
#3705=VECTOR('',#13071,0.4);
#3706=VECTOR('',#13076,0.425);
#3707=VECTOR('',#13081,0.41);
#3708=VECTOR('',#13090,0.26);
#3709=VECTOR('',#13095,0.25);
#3710=VECTOR('',#13100,0.225);
#3711=VECTOR('',#13105,1.);
#3712=VECTOR('',#13106,1.);
#3713=VECTOR('',#13107,1.);
#3714=VECTOR('',#13108,1.);
#3715=VECTOR('',#13111,1.);
#3716=VECTOR('',#13112,1.);
#3717=VECTOR('',#13113,1.);
#3718=VECTOR('',#13116,1.);
#3719=VECTOR('',#13117,1.);
#3720=VECTOR('',#13118,1.);
#3721=VECTOR('',#13121,1.);
#3722=VECTOR('',#13122,1.);
#3723=VECTOR('',#13123,1.);
#3724=VECTOR('',#13126,1.);
#3725=VECTOR('',#13127,1.);
#3726=VECTOR('',#13128,1.);
#3727=VECTOR('',#13131,1.);
#3728=VECTOR('',#13132,1.);
#4137=CIRCLE('',#10443,0.375);
#4138=CIRCLE('',#10445,0.425);
#4139=CIRCLE('',#10447,0.425);
#4140=CIRCLE('',#10449,0.395);
#4141=CIRCLE('',#10451,0.27);
#4142=CIRCLE('',#10453,0.24505);
#4143=CIRCLE('',#10455,0.24505);
#4144=CIRCLE('',#10457,0.2);
#4857=VERTEX_POINT('',#16585);
#4858=VERTEX_POINT('',#16588);
#4859=VERTEX_POINT('',#16592);
#4860=VERTEX_POINT('',#16596);
#4861=VERTEX_POINT('',#16600);
#4862=VERTEX_POINT('',#16603);
#4863=VERTEX_POINT('',#16607);
#4864=VERTEX_POINT('',#16611);
#4865=VERTEX_POINT('',#16616);
#4866=VERTEX_POINT('',#16617);
#4867=VERTEX_POINT('',#16619);
#4868=VERTEX_POINT('',#16621);
#4869=VERTEX_POINT('',#16625);
#4870=VERTEX_POINT('',#16627);
#4871=VERTEX_POINT('',#16631);
#4872=VERTEX_POINT('',#16633);
#4873=VERTEX_POINT('',#16637);
#4874=VERTEX_POINT('',#16639);
#4875=VERTEX_POINT('',#16643);
#4876=VERTEX_POINT('',#16645);
#5934=EDGE_CURVE('',#4857,#4857,#4137,.T.);
#5935=EDGE_CURVE('',#4858,#4858,#4138,.T.);
#5936=EDGE_CURVE('',#4858,#4857,#3059,.T.);
#5937=EDGE_CURVE('',#4859,#4859,#4139,.T.);
#5938=EDGE_CURVE('',#4859,#4858,#3060,.T.);
#5939=EDGE_CURVE('',#4860,#4860,#4140,.T.);
#5940=EDGE_CURVE('',#4860,#4859,#3061,.T.);
#5941=EDGE_CURVE('',#4861,#4861,#4141,.T.);
#5942=EDGE_CURVE('',#4862,#4862,#4142,.F.);
#5943=EDGE_CURVE('',#4862,#4861,#3062,.T.);
#5944=EDGE_CURVE('',#4863,#4863,#4143,.F.);
#5945=EDGE_CURVE('',#4863,#4862,#3063,.T.);
#5946=EDGE_CURVE('',#4864,#4864,#4144,.T.);
#5947=EDGE_CURVE('',#4864,#4863,#3064,.T.);
#5948=EDGE_CURVE('',#4865,#4866,#3065,.T.);
#5949=EDGE_CURVE('',#4866,#4867,#3066,.T.);
#5950=EDGE_CURVE('',#4867,#4868,#3067,.T.);
#5951=EDGE_CURVE('',#4865,#4868,#3068,.T.);
#5952=EDGE_CURVE('',#4866,#4869,#3069,.T.);
#5953=EDGE_CURVE('',#4869,#4870,#3070,.T.);
#5954=EDGE_CURVE('',#4870,#4867,#3071,.T.);
#5955=EDGE_CURVE('',#4869,#4871,#3072,.T.);
#5956=EDGE_CURVE('',#4871,#4872,#3073,.T.);
#5957=EDGE_CURVE('',#4872,#4870,#3074,.T.);
#5958=EDGE_CURVE('',#4871,#4873,#3075,.T.);
#5959=EDGE_CURVE('',#4873,#4874,#3076,.T.);
#5960=EDGE_CURVE('',#4874,#4872,#3077,.T.);
#5961=EDGE_CURVE('',#4873,#4875,#3078,.T.);
#5962=EDGE_CURVE('',#4875,#4876,#3079,.T.);
#5963=EDGE_CURVE('',#4876,#4874,#3080,.T.);
#5964=EDGE_CURVE('',#4875,#4865,#3081,.T.);
#5965=EDGE_CURVE('',#4868,#4876,#3082,.T.);
#8072=ORIENTED_EDGE('',*,*,#5934,.F.);
#8073=ORIENTED_EDGE('',*,*,#5935,.F.);
#8074=ORIENTED_EDGE('',*,*,#5936,.T.);
#8075=ORIENTED_EDGE('',*,*,#5934,.T.);
#8076=ORIENTED_EDGE('',*,*,#5936,.F.);
#8077=ORIENTED_EDGE('',*,*,#5937,.F.);
#8078=ORIENTED_EDGE('',*,*,#5938,.T.);
#8079=ORIENTED_EDGE('',*,*,#5935,.T.);
#8080=ORIENTED_EDGE('',*,*,#5938,.F.);
#8081=ORIENTED_EDGE('',*,*,#5939,.F.);
#8082=ORIENTED_EDGE('',*,*,#5940,.T.);
#8083=ORIENTED_EDGE('',*,*,#5937,.T.);
#8084=ORIENTED_EDGE('',*,*,#5940,.F.);
#8085=ORIENTED_EDGE('',*,*,#5939,.T.);
#8086=ORIENTED_EDGE('',*,*,#5941,.F.);
#8087=ORIENTED_EDGE('',*,*,#5942,.F.);
#8088=ORIENTED_EDGE('',*,*,#5943,.T.);
#8089=ORIENTED_EDGE('',*,*,#5941,.T.);
#8090=ORIENTED_EDGE('',*,*,#5943,.F.);
#8091=ORIENTED_EDGE('',*,*,#5944,.F.);
#8092=ORIENTED_EDGE('',*,*,#5945,.T.);
#8093=ORIENTED_EDGE('',*,*,#5942,.T.);
#8094=ORIENTED_EDGE('',*,*,#5945,.F.);
#8095=ORIENTED_EDGE('',*,*,#5946,.F.);
#8096=ORIENTED_EDGE('',*,*,#5947,.T.);
#8097=ORIENTED_EDGE('',*,*,#5944,.T.);
#8098=ORIENTED_EDGE('',*,*,#5947,.F.);
#8099=ORIENTED_EDGE('',*,*,#5946,.T.);
#8100=ORIENTED_EDGE('',*,*,#5948,.T.);
#8101=ORIENTED_EDGE('',*,*,#5949,.T.);
#8102=ORIENTED_EDGE('',*,*,#5950,.T.);
#8103=ORIENTED_EDGE('',*,*,#5951,.F.);
#8104=ORIENTED_EDGE('',*,*,#5952,.T.);
#8105=ORIENTED_EDGE('',*,*,#5953,.T.);
#8106=ORIENTED_EDGE('',*,*,#5954,.T.);
#8107=ORIENTED_EDGE('',*,*,#5949,.F.);
#8108=ORIENTED_EDGE('',*,*,#5955,.T.);
#8109=ORIENTED_EDGE('',*,*,#5956,.T.);
#8110=ORIENTED_EDGE('',*,*,#5957,.T.);
#8111=ORIENTED_EDGE('',*,*,#5953,.F.);
#8112=ORIENTED_EDGE('',*,*,#5958,.T.);
#8113=ORIENTED_EDGE('',*,*,#5959,.T.);
#8114=ORIENTED_EDGE('',*,*,#5960,.T.);
#8115=ORIENTED_EDGE('',*,*,#5956,.F.);
#8116=ORIENTED_EDGE('',*,*,#5961,.T.);
#8117=ORIENTED_EDGE('',*,*,#5962,.T.);
#8118=ORIENTED_EDGE('',*,*,#5963,.T.);
#8119=ORIENTED_EDGE('',*,*,#5959,.F.);
#8120=ORIENTED_EDGE('',*,*,#5964,.T.);
#8121=ORIENTED_EDGE('',*,*,#5951,.T.);
#8122=ORIENTED_EDGE('',*,*,#5965,.T.);
#8123=ORIENTED_EDGE('',*,*,#5962,.F.);
#8124=ORIENTED_EDGE('',*,*,#5964,.F.);
#8125=ORIENTED_EDGE('',*,*,#5961,.F.);
#8126=ORIENTED_EDGE('',*,*,#5958,.F.);
#8127=ORIENTED_EDGE('',*,*,#5955,.F.);
#8128=ORIENTED_EDGE('',*,*,#5952,.F.);
#8129=ORIENTED_EDGE('',*,*,#5948,.F.);
#8130=ORIENTED_EDGE('',*,*,#5965,.F.);
#8131=ORIENTED_EDGE('',*,*,#5950,.F.);
#8132=ORIENTED_EDGE('',*,*,#5954,.F.);
#8133=ORIENTED_EDGE('',*,*,#5957,.F.);
#8134=ORIENTED_EDGE('',*,*,#5960,.F.);
#8135=ORIENTED_EDGE('',*,*,#5963,.F.);
#8351=CYLINDRICAL_SURFACE('',#10446,0.425);
#8352=CYLINDRICAL_SURFACE('',#10454,0.24505);
#8845=ADVANCED_FACE('',(#1707),#1195,.T.);
#8846=ADVANCED_FACE('',(#1708),#30,.T.);
#8847=ADVANCED_FACE('',(#1709),#8351,.T.);
#8848=ADVANCED_FACE('',(#1710),#31,.T.);
#8849=ADVANCED_FACE('',(#1711,#895),#1196,.T.);
#8850=ADVANCED_FACE('',(#1712),#32,.T.);
#8851=ADVANCED_FACE('',(#1713),#8352,.T.);
#8852=ADVANCED_FACE('',(#1714),#33,.T.);
#8853=ADVANCED_FACE('',(#1715),#1197,.T.);
#8854=ADVANCED_FACE('',(#1716),#1198,.F.);
#8855=ADVANCED_FACE('',(#1717),#1199,.F.);
#8856=ADVANCED_FACE('',(#1718),#1200,.F.);
#8857=ADVANCED_FACE('',(#1719),#1201,.F.);
#8858=ADVANCED_FACE('',(#1720),#1202,.F.);
#8859=ADVANCED_FACE('',(#1721),#1203,.F.);
#8860=ADVANCED_FACE('',(#1722),#1204,.F.);
#8861=ADVANCED_FACE('',(#1723),#1205,.F.);
#8938=CLOSED_SHELL('',(#8845,#8846,#8847,#8848,#8849,#8850,#8851,#8852,
#8853));
#8939=CLOSED_SHELL('',(#8854,#8855,#8856,#8857,#8858,#8859,#8860,#8861));
#10441=AXIS2_PLACEMENT_3D('',#16583,#13061,#13062);
#10442=AXIS2_PLACEMENT_3D('',#16584,#13063,#13064);
#10443=AXIS2_PLACEMENT_3D('',#16586,#13065,#13066);
#10444=AXIS2_PLACEMENT_3D('',#16587,#13067,#13068);
#10445=AXIS2_PLACEMENT_3D('',#16589,#13069,#13070);
#10446=AXIS2_PLACEMENT_3D('',#16591,#13072,#13073);
#10447=AXIS2_PLACEMENT_3D('',#16593,#13074,#13075);
#10448=AXIS2_PLACEMENT_3D('',#16595,#13077,#13078);
#10449=AXIS2_PLACEMENT_3D('',#16597,#13079,#13080);
#10450=AXIS2_PLACEMENT_3D('',#16599,#13082,#13083);
#10451=AXIS2_PLACEMENT_3D('',#16601,#13084,#13085);
#10452=AXIS2_PLACEMENT_3D('',#16602,#13086,#13087);
#10453=AXIS2_PLACEMENT_3D('',#16604,#13088,#13089);
#10454=AXIS2_PLACEMENT_3D('',#16606,#13091,#13092);
#10455=AXIS2_PLACEMENT_3D('',#16608,#13093,#13094);
#10456=AXIS2_PLACEMENT_3D('',#16610,#13096,#13097);
#10457=AXIS2_PLACEMENT_3D('',#16612,#13098,#13099);
#10458=AXIS2_PLACEMENT_3D('',#16614,#13101,#13102);
#10459=AXIS2_PLACEMENT_3D('',#16615,#13103,#13104);
#10460=AXIS2_PLACEMENT_3D('',#16624,#13109,#13110);
#10461=AXIS2_PLACEMENT_3D('',#16630,#13114,#13115);
#10462=AXIS2_PLACEMENT_3D('',#16636,#13119,#13120);
#10463=AXIS2_PLACEMENT_3D('',#16642,#13124,#13125);
#10464=AXIS2_PLACEMENT_3D('',#16648,#13129,#13130);
#10465=AXIS2_PLACEMENT_3D('',#16651,#13133,#13134);
#10466=AXIS2_PLACEMENT_3D('',#16652,#13135,#13136);
#13061=DIRECTION('axis',(0.,0.,1.));
#13062=DIRECTION('refdir',(1.,0.,0.));
#13063=DIRECTION('center_axis',(0.,1.,0.));
#13064=DIRECTION('ref_axis',(0.,0.,1.));
#13065=DIRECTION('center_axis',(0.,-1.,0.));
#13066=DIRECTION('ref_axis',(1.,0.,0.));
#13067=DIRECTION('center_axis',(0.,-1.,0.));
#13068=DIRECTION('ref_axis',(1.,0.,0.));
#13069=DIRECTION('center_axis',(0.,-1.,0.));
#13070=DIRECTION('ref_axis',(1.,0.,0.));
#13071=DIRECTION('',(0.707106781186548,0.707106781186547,8.65956056235493E-17));
#13072=DIRECTION('center_axis',(0.,-1.,0.));
#13073=DIRECTION('ref_axis',(1.,0.,0.));
#13074=DIRECTION('center_axis',(0.,-1.,0.));
#13075=DIRECTION('ref_axis',(1.,0.,0.));
#13076=DIRECTION('',(0.,1.,0.));
#13077=DIRECTION('center_axis',(0.,1.,0.));
#13078=DIRECTION('ref_axis',(1.,0.,0.));
#13079=DIRECTION('center_axis',(0.,-1.,0.));
#13080=DIRECTION('ref_axis',(1.,0.,0.));
#13081=DIRECTION('',(-0.707106781186547,0.707106781186548,-8.65956056235493E-17));
#13082=DIRECTION('center_axis',(0.,-1.,0.));
#13083=DIRECTION('ref_axis',(0.,0.,-1.));
#13084=DIRECTION('center_axis',(0.,-1.,0.));
#13085=DIRECTION('ref_axis',(1.,0.,0.));
#13086=DIRECTION('center_axis',(0.,1.,0.));
#13087=DIRECTION('ref_axis',(1.,0.,0.));
#13088=DIRECTION('center_axis',(0.,1.,0.));
#13089=DIRECTION('ref_axis',(1.,0.,0.));
#13090=DIRECTION('',(-0.447213595499958,0.894427190999916,-5.47678698264203E-17));
#13091=DIRECTION('center_axis',(0.,-1.,0.));
#13092=DIRECTION('ref_axis',(1.,0.,0.));
#13093=DIRECTION('center_axis',(0.,1.,0.));
#13094=DIRECTION('ref_axis',(1.,0.,0.));
#13095=DIRECTION('',(0.,1.,0.));
#13096=DIRECTION('center_axis',(0.,1.,0.));
#13097=DIRECTION('ref_axis',(1.,0.,0.));
#13098=DIRECTION('center_axis',(0.,-1.,0.));
#13099=DIRECTION('ref_axis',(1.,0.,0.));
#13100=DIRECTION('',(-0.707106781186547,0.707106781186548,-8.65956056235493E-17));
#13101=DIRECTION('center_axis',(0.,-1.,0.));
#13102=DIRECTION('ref_axis',(0.,0.,-1.));
#13103=DIRECTION('center_axis',(0.866025403784439,0.,-0.5));
#13104=DIRECTION('ref_axis',(0.5,0.,0.866025403784439));
#13105=DIRECTION('',(-0.5,0.,-0.866025403784439));
#13106=DIRECTION('',(0.,-1.,0.));
#13107=DIRECTION('',(0.5,0.,0.866025403784439));
#13108=DIRECTION('',(0.,-1.,0.));
#13109=DIRECTION('center_axis',(1.20185167898973E-16,0.,-1.));
#13110=DIRECTION('ref_axis',(1.,0.,1.20185167898973E-16));
#13111=DIRECTION('',(-1.,0.,-1.20185167898973E-16));
#13112=DIRECTION('',(0.,-1.,0.));
#13113=DIRECTION('',(1.,0.,1.20185167898973E-16));
#13114=DIRECTION('center_axis',(-0.866025403784439,0.,-0.5));
#13115=DIRECTION('ref_axis',(0.5,0.,-0.866025403784439));
#13116=DIRECTION('',(-0.5,0.,0.866025403784439));
#13117=DIRECTION('',(0.,-1.,0.));
#13118=DIRECTION('',(0.5,0.,-0.866025403784439));
#13119=DIRECTION('center_axis',(-0.866025403784439,0.,0.5));
#13120=DIRECTION('ref_axis',(-0.5,0.,-0.866025403784439));
#13121=DIRECTION('',(0.5,0.,0.866025403784439));
#13122=DIRECTION('',(0.,-1.,0.));
#13123=DIRECTION('',(-0.5,0.,-0.866025403784439));
#13124=DIRECTION('center_axis',(-2.40370335797945E-16,0.,1.));
#13125=DIRECTION('ref_axis',(-1.,0.,-2.40370335797945E-16));
#13126=DIRECTION('',(1.,0.,2.40370335797945E-16));
#13127=DIRECTION('',(0.,-1.,0.));
#13128=DIRECTION('',(-1.,0.,-2.40370335797945E-16));
#13129=DIRECTION('center_axis',(0.866025403784439,0.,0.5));
#13130=DIRECTION('ref_axis',(-0.5,0.,0.866025403784439));
#13131=DIRECTION('',(0.5,0.,-0.866025403784439));
#13132=DIRECTION('',(-0.5,0.,0.866025403784439));
#13133=DIRECTION('center_axis',(0.,1.,0.));
#13134=DIRECTION('ref_axis',(1.,0.,0.));
#13135=DIRECTION('center_axis',(0.,-1.,0.));
#13136=DIRECTION('ref_axis',(0.,0.,-1.));
#16583=CARTESIAN_POINT('',(0.,0.,0.));
#16584=CARTESIAN_POINT('Origin',(0.375,0.5,0.));
#16585=CARTESIAN_POINT('',(-0.375,0.5,-4.59242549680257E-17));
#16586=CARTESIAN_POINT('Origin',(0.,0.5,0.));
#16587=CARTESIAN_POINT('Origin',(0.,0.475,0.));
#16588=CARTESIAN_POINT('',(-0.425,0.45,-5.20474889637625E-17));
#16589=CARTESIAN_POINT('Origin',(0.,0.45,0.));
#16590=CARTESIAN_POINT('',(-0.4,0.475,-4.89858719658941E-17));
#16591=CARTESIAN_POINT('Origin',(0.,0.24,0.));
#16592=CARTESIAN_POINT('',(-0.425,0.0299999999999998,-5.20474889637625E-17));
#16593=CARTESIAN_POINT('Origin',(0.,0.0299999999999998,0.));
#16594=CARTESIAN_POINT('',(-0.425,0.24,-5.20474889637625E-17));
#16595=CARTESIAN_POINT('Origin',(0.,0.0150000000000001,0.));
#16596=CARTESIAN_POINT('',(-0.395,4.85722573273506E-17,-4.83735485663204E-17));
#16597=CARTESIAN_POINT('Origin',(0.,0.,0.));
#16598=CARTESIAN_POINT('',(-0.41,0.0150000000000001,-5.02105187650415E-17));
#16599=CARTESIAN_POINT('Origin',(0.27,0.,0.));
#16600=CARTESIAN_POINT('',(-0.27,0.,-3.30654635769785E-17));
#16601=CARTESIAN_POINT('Origin',(0.,0.,0.));
#16602=CARTESIAN_POINT('Origin',(0.,-0.02,0.));
#16603=CARTESIAN_POINT('',(-0.24505,-0.0498999999999999,3.00099698131059E-17));
#16604=CARTESIAN_POINT('Origin',(0.,-0.0498999999999999,0.));
#16605=CARTESIAN_POINT('',(-0.26,-0.02,-3.18408167778312E-17));
#16606=CARTESIAN_POINT('Origin',(0.,-0.995,0.));
#16607=CARTESIAN_POINT('',(-0.24505,-1.95495,3.00099698131059E-17));
#16608=CARTESIAN_POINT('Origin',(0.,-1.95495,0.));
#16609=CARTESIAN_POINT('',(-0.24505,-0.995,-3.00099698131059E-17));
#16610=CARTESIAN_POINT('Origin',(0.,-1.975,0.));
#16611=CARTESIAN_POINT('',(-0.2,-2.,-2.44929359829471E-17));
#16612=CARTESIAN_POINT('Origin',(0.,-2.,0.));
#16613=CARTESIAN_POINT('',(-0.225,-1.975,-2.75545529808154E-17));
#16614=CARTESIAN_POINT('Origin',(0.,-2.,0.));
#16615=CARTESIAN_POINT('Origin',(0.115470053837925,-0.5,-0.2));
#16616=CARTESIAN_POINT('',(0.23094010767585,-0.5,0.));
#16617=CARTESIAN_POINT('',(0.115470053837925,-0.5,-0.2));
#16618=CARTESIAN_POINT('',(0.23094010767585,-0.5,0.));
#16619=CARTESIAN_POINT('',(0.115470053837925,-0.8,-0.2));
#16620=CARTESIAN_POINT('',(0.115470053837925,-0.5,-0.2));
#16621=CARTESIAN_POINT('',(0.23094010767585,-0.8,0.));
#16622=CARTESIAN_POINT('',(0.23094010767585,-0.8,0.));
#16623=CARTESIAN_POINT('',(0.23094010767585,-0.5,0.));
#16624=CARTESIAN_POINT('Origin',(-0.115470053837925,-0.5,-0.2));
#16625=CARTESIAN_POINT('',(-0.115470053837925,-0.5,-0.2));
#16626=CARTESIAN_POINT('',(0.115470053837925,-0.5,-0.2));
#16627=CARTESIAN_POINT('',(-0.115470053837925,-0.8,-0.2));
#16628=CARTESIAN_POINT('',(-0.115470053837925,-0.5,-0.2));
#16629=CARTESIAN_POINT('',(0.115470053837925,-0.8,-0.2));
#16630=CARTESIAN_POINT('Origin',(-0.23094010767585,-0.5,-2.77555756156289E-17));
#16631=CARTESIAN_POINT('',(-0.23094010767585,-0.5,-2.82820063659975E-17));
#16632=CARTESIAN_POINT('',(-0.115470053837925,-0.5,-0.2));
#16633=CARTESIAN_POINT('',(-0.23094010767585,-0.8,-2.77555756156289E-17));
#16634=CARTESIAN_POINT('',(-0.23094010767585,-0.5,-2.82820063659975E-17));
#16635=CARTESIAN_POINT('',(-0.115470053837925,-0.8,-0.2));
#16636=CARTESIAN_POINT('Origin',(-0.115470053837925,-0.5,0.2));
#16637=CARTESIAN_POINT('',(-0.115470053837925,-0.5,0.2));
#16638=CARTESIAN_POINT('',(-0.23094010767585,-0.5,-2.82820063659975E-17));
#16639=CARTESIAN_POINT('',(-0.115470053837925,-0.8,0.2));
#16640=CARTESIAN_POINT('',(-0.115470053837925,-0.5,0.2));
#16641=CARTESIAN_POINT('',(-0.23094010767585,-0.8,-2.82820063659975E-17));
#16642=CARTESIAN_POINT('Origin',(0.115470053837925,-0.5,0.2));
#16643=CARTESIAN_POINT('',(0.115470053837925,-0.5,0.2));
#16644=CARTESIAN_POINT('',(-0.115470053837925,-0.5,0.2));
#16645=CARTESIAN_POINT('',(0.115470053837925,-0.8,0.2));
#16646=CARTESIAN_POINT('',(0.115470053837925,-0.5,0.2));
#16647=CARTESIAN_POINT('',(-0.115470053837925,-0.8,0.2));
#16648=CARTESIAN_POINT('Origin',(0.23094010767585,-0.5,0.));
#16649=CARTESIAN_POINT('',(0.115470053837925,-0.5,0.2));
#16650=CARTESIAN_POINT('',(0.115470053837925,-0.8,0.2));
#16651=CARTESIAN_POINT('Origin',(0.,-0.5,0.));
#16652=CARTESIAN_POINT('Origin',(0.,-0.8,0.));
#16850=UNCERTAINTY_MEASURE_WITH_UNIT(LENGTH_MEASURE(0.001),#16912,
'DISTANCE_ACCURACY_VALUE',
'Maximum model space distance between geometric entities at asserted c
onnectivities');
#16852=UNCERTAINTY_MEASURE_WITH_UNIT(LENGTH_MEASURE(0.001),#16912,
'DISTANCE_ACCURACY_VALUE',
'Maximum model space distance between geometric entities at asserted c
onnectivities');
#16909=(
GEOMETRIC_REPRESENTATION_CONTEXT(3)
GLOBAL_UNCERTAINTY_ASSIGNED_CONTEXT((#16850))
GLOBAL_UNIT_ASSIGNED_CONTEXT((#16912,#16914,#16915))
REPRESENTATION_CONTEXT('','3D')
);
#16911=(
GEOMETRIC_REPRESENTATION_CONTEXT(3)
GLOBAL_UNCERTAINTY_ASSIGNED_CONTEXT((#16852))
GLOBAL_UNIT_ASSIGNED_CONTEXT((#16912,#16914,#16915))
REPRESENTATION_CONTEXT('','3D')
);
#16912=(
LENGTH_UNIT()
NAMED_UNIT(*)
SI_UNIT(.CENTI.,.METRE.)
);
#16914=(
NAMED_UNIT(*)
PLANE_ANGLE_UNIT()
SI_UNIT($,.RADIAN.)
);
#16915=(
NAMED_UNIT(*)
SI_UNIT($,.STERADIAN.)
SOLID_ANGLE_UNIT()
);
#16972=SHAPE_DEFINITION_REPRESENTATION(#17047,#17180);
#17047=PRODUCT_DEFINITION_SHAPE('',$,#17239);
#17180=SHAPE_REPRESENTATION('',(#10441),#16909);
#17182=PRODUCT_DEFINITION_CONTEXT('part definition',#17358,'design');
#17239=PRODUCT_DEFINITION('Cap Screw - M5x20','Cap Screw - M5x20',#17297,
#17182);
#17297=PRODUCT_DEFINITION_FORMATION('',$,#17416);
#17358=APPLICATION_CONTEXT(
'Core Data for Automotive Mechanical Design Process');
#17359=PRODUCT_CONTEXT('part definition',#17358,'mechanical');
#17416=PRODUCT('Cap Screw - M5x20','Cap Screw - M5x20',
'Cap Screw - M5x20',(#17359));
#17488=COLOUR_RGB('Black',0.12,0.14,0.17);
#17489=FILL_AREA_STYLE_COLOUR('',#17488);
#17490=FILL_AREA_STYLE('',(#17489));
#17491=SURFACE_STYLE_FILL_AREA(#17490);
#17492=SURFACE_SIDE_STYLE('',(#17491));
#17493=SURFACE_STYLE_USAGE(.BOTH.,#17492);
#17494=PRESENTATION_STYLE_ASSIGNMENT((#17493));
ENDSEC;
END-ISO-10303-21;
